ISO-10303-21;
HEADER;
/* Generated by software containing ST-Developer
 * from STEP Tools, Inc. (www.steptools.com) 
 */

FILE_DESCRIPTION(
/* description */ ('STEP AP214'),
/* implementation_level */ '2;1');

FILE_NAME(
/* name */ 'PRT-TQ-1012-04.step',
/* time_stamp */ '2026-10-07T12:49:37-07:00',
/* author */ (''),
/* organization */ (''),
/* preprocessor_version */ 'ST-DEVELOPER v20.2',
/* originating_system */ 'Autodesk Translation Framework v15.15.0.0',
/* authorisation */ '');

FILE_SCHEMA (('AUTOMOTIVE_DESIGN { 1 0 10303 214 3 1 1 }'));
ENDSEC;

DATA;
#10=MECHANICAL_DESIGN_GEOMETRIC_PRESENTATION_REPRESENTATION('',(#313),#33016);
#255=SHAPE_REPRESENTATION_RELATIONSHIP('SRR','None',#33150,#282);
#282=ADVANCED_BREP_SHAPE_REPRESENTATION('',(#340),#33011);
#313=STYLED_ITEM('',(#33284),#340);
#340=MANIFOLD_SOLID_BREP('Body1',#9964);
#365=CONICAL_SURFACE('',#11122,16.,0.244978663126864);
#366=CONICAL_SURFACE('',#11133,14.1,0.78539816339745);
#367=CONICAL_SURFACE('',#11139,13.1,0.837758040957281);
#404=TOROIDAL_SURFACE('',#11119,61.9943178149179,45.);
#546=FACE_BOUND('',#2157,.T.);
#547=FACE_BOUND('',#2162,.T.);
#548=FACE_BOUND('',#2165,.T.);
#549=FACE_BOUND('',#2172,.T.);
#1004=PLANE('',#11114);
#1005=PLANE('',#11124);
#1006=PLANE('',#11128);
#1007=PLANE('',#11144);
#1528=FACE_OUTER_BOUND('',#2156,.T.);
#1529=FACE_OUTER_BOUND('',#2158,.T.);
#1530=FACE_OUTER_BOUND('',#2159,.T.);
#1531=FACE_OUTER_BOUND('',#2160,.T.);
#1532=FACE_OUTER_BOUND('',#2161,.T.);
#1533=FACE_OUTER_BOUND('',#2163,.T.);
#1534=FACE_OUTER_BOUND('',#2164,.T.);
#1535=FACE_OUTER_BOUND('',#2166,.T.);
#1536=FACE_OUTER_BOUND('',#2167,.T.);
#1537=FACE_OUTER_BOUND('',#2168,.T.);
#1538=FACE_OUTER_BOUND('',#2169,.T.);
#1539=FACE_OUTER_BOUND('',#2170,.T.);
#1540=FACE_OUTER_BOUND('',#2171,.T.);
#1541=FACE_OUTER_BOUND('',#2173,.T.);
#2156=EDGE_LOOP('',(#9008));
#2157=EDGE_LOOP('',(#9009));
#2158=EDGE_LOOP('',(#9010,#9011,#9012,#9013));
#2159=EDGE_LOOP('',(#9014,#9015,#9016,#9017));
#2160=EDGE_LOOP('',(#9018,#9019,#9020,#9021));
#2161=EDGE_LOOP('',(#9022));
#2162=EDGE_LOOP('',(#9023));
#2163=EDGE_LOOP('',(#9024,#9025,#9026,#9027));
#2164=EDGE_LOOP('',(#9028));
#2165=EDGE_LOOP('',(#9029));
#2166=EDGE_LOOP('',(#9030,#9031,#9032,#9033,#9034));
#2167=EDGE_LOOP('',(#9035,#9036,#9037,#9038,#9039,#9040));
#2168=EDGE_LOOP('',(#9041,#9042,#9043,#9044,#9045,#9046));
#2169=EDGE_LOOP('',(#9047,#9048,#9049,#9050,#9051,#9052));
#2170=EDGE_LOOP('',(#9053,#9054,#9055,#9056,#9057));
#2171=EDGE_LOOP('',(#9058));
#2172=EDGE_LOOP('',(#9059));
#2173=EDGE_LOOP('',(#9060,#9061,#9062,#9063));
#2552=CIRCLE('',#11115,19.);
#2553=CIRCLE('',#11116,16.1);
#2554=CIRCLE('',#11118,19.);
#2555=CIRCLE('',#11120,45.);
#2556=CIRCLE('',#11121,17.);
#2557=CIRCLE('',#11123,16.);
#2558=CIRCLE('',#11125,13.1);
#2559=CIRCLE('',#11127,13.1);
#2560=CIRCLE('',#11129,15.1);
#2561=CIRCLE('',#11131,15.1);
#2562=CIRCLE('',#11132,15.1);
#2563=CIRCLE('',#11134,14.1);
#2564=CIRCLE('',#11135,14.1);
#2565=CIRCLE('',#11137,14.1);
#2566=CIRCLE('',#11138,14.1);
#2567=CIRCLE('',#11140,13.1);
#2568=CIRCLE('',#11141,13.1);
#2569=CIRCLE('',#11143,13.1);
#2570=CIRCLE('',#11145,16.1);
#3315=LINE('',#32663,#4065);
#3316=LINE('',#32671,#4066);
#3317=LINE('',#32678,#4067);
#3318=LINE('',#32685,#4068);
#3319=LINE('',#32694,#4069);
#3320=LINE('',#32697,#4070);
#3321=LINE('',#32706,#4071);
#3322=LINE('',#32709,#4072);
#3323=LINE('',#32715,#4073);
#4065=VECTOR('',#13650,19.);
#4066=VECTOR('',#13661,16.);
#4067=VECTOR('',#13670,13.1);
#4068=VECTOR('',#13679,15.1);
#4069=VECTOR('',#13690,14.1);
#4070=VECTOR('',#13693,14.1);
#4071=VECTOR('',#13704,13.1);
#4072=VECTOR('',#13707,13.1);
#4073=VECTOR('',#13716,16.1);
#4954=VERTEX_POINT('',#32657);
#4955=VERTEX_POINT('',#32659);
#4956=VERTEX_POINT('',#32662);
#4957=VERTEX_POINT('',#32666);
#4958=VERTEX_POINT('',#32670);
#4959=VERTEX_POINT('',#32674);
#4960=VERTEX_POINT('',#32677);
#4961=VERTEX_POINT('',#32681);
#4962=VERTEX_POINT('',#32684);
#4963=VERTEX_POINT('',#32686);
#4964=VERTEX_POINT('',#32690);
#4965=VERTEX_POINT('',#32691);
#4966=VERTEX_POINT('',#32696);
#4967=VERTEX_POINT('',#32698);
#4968=VERTEX_POINT('',#32702);
#4969=VERTEX_POINT('',#32703);
#4970=VERTEX_POINT('',#32708);
#4971=VERTEX_POINT('',#32712);
#6317=EDGE_CURVE('',#4954,#4954,#2552,.T.);
#6318=EDGE_CURVE('',#4955,#4955,#2553,.T.);
#6319=EDGE_CURVE('',#4954,#4956,#3315,.T.);
#6320=EDGE_CURVE('',#4956,#4956,#2554,.T.);
#6321=EDGE_CURVE('',#4956,#4957,#2555,.T.);
#6322=EDGE_CURVE('',#4957,#4957,#2556,.T.);
#6323=EDGE_CURVE('',#4957,#4958,#3316,.T.);
#6324=EDGE_CURVE('',#4958,#4958,#2557,.T.);
#6325=EDGE_CURVE('',#4959,#4959,#2558,.T.);
#6326=EDGE_CURVE('',#4959,#4960,#3317,.T.);
#6327=EDGE_CURVE('',#4960,#4960,#2559,.T.);
#6328=EDGE_CURVE('',#4961,#4961,#2560,.T.);
#6329=EDGE_CURVE('',#4961,#4962,#3318,.T.);
#6330=EDGE_CURVE('',#4962,#4963,#2561,.T.);
#6331=EDGE_CURVE('',#4963,#4962,#2562,.T.);
#6332=EDGE_CURVE('',#4964,#4965,#2563,.T.);
#6333=EDGE_CURVE('',#4965,#4964,#2564,.T.);
#6334=EDGE_CURVE('',#4964,#4963,#3319,.T.);
#6335=EDGE_CURVE('',#4965,#4966,#3320,.T.);
#6336=EDGE_CURVE('',#4966,#4967,#2565,.T.);
#6337=EDGE_CURVE('',#4967,#4966,#2566,.T.);
#6338=EDGE_CURVE('',#4968,#4969,#2567,.T.);
#6339=EDGE_CURVE('',#4969,#4968,#2568,.T.);
#6340=EDGE_CURVE('',#4968,#4967,#3321,.T.);
#6341=EDGE_CURVE('',#4969,#4970,#3322,.T.);
#6342=EDGE_CURVE('',#4970,#4970,#2569,.T.);
#6343=EDGE_CURVE('',#4971,#4971,#2570,.T.);
#6344=EDGE_CURVE('',#4971,#4955,#3323,.T.);
#9008=ORIENTED_EDGE('',*,*,#6317,.T.);
#9009=ORIENTED_EDGE('',*,*,#6318,.F.);
#9010=ORIENTED_EDGE('',*,*,#6317,.F.);
#9011=ORIENTED_EDGE('',*,*,#6319,.T.);
#9012=ORIENTED_EDGE('',*,*,#6320,.T.);
#9013=ORIENTED_EDGE('',*,*,#6319,.F.);
#9014=ORIENTED_EDGE('',*,*,#6320,.F.);
#9015=ORIENTED_EDGE('',*,*,#6321,.T.);
#9016=ORIENTED_EDGE('',*,*,#6322,.T.);
#9017=ORIENTED_EDGE('',*,*,#6321,.F.);
#9018=ORIENTED_EDGE('',*,*,#6322,.F.);
#9019=ORIENTED_EDGE('',*,*,#6323,.T.);
#9020=ORIENTED_EDGE('',*,*,#6324,.T.);
#9021=ORIENTED_EDGE('',*,*,#6323,.F.);
#9022=ORIENTED_EDGE('',*,*,#6324,.F.);
#9023=ORIENTED_EDGE('',*,*,#6325,.T.);
#9024=ORIENTED_EDGE('',*,*,#6325,.F.);
#9025=ORIENTED_EDGE('',*,*,#6326,.T.);
#9026=ORIENTED_EDGE('',*,*,#6327,.T.);
#9027=ORIENTED_EDGE('',*,*,#6326,.F.);
#9028=ORIENTED_EDGE('',*,*,#6328,.T.);
#9029=ORIENTED_EDGE('',*,*,#6327,.F.);
#9030=ORIENTED_EDGE('',*,*,#6328,.F.);
#9031=ORIENTED_EDGE('',*,*,#6329,.T.);
#9032=ORIENTED_EDGE('',*,*,#6330,.T.);
#9033=ORIENTED_EDGE('',*,*,#6331,.T.);
#9034=ORIENTED_EDGE('',*,*,#6329,.F.);
#9035=ORIENTED_EDGE('',*,*,#6332,.T.);
#9036=ORIENTED_EDGE('',*,*,#6333,.T.);
#9037=ORIENTED_EDGE('',*,*,#6334,.T.);
#9038=ORIENTED_EDGE('',*,*,#6330,.F.);
#9039=ORIENTED_EDGE('',*,*,#6331,.F.);
#9040=ORIENTED_EDGE('',*,*,#6334,.F.);
#9041=ORIENTED_EDGE('',*,*,#6332,.F.);
#9042=ORIENTED_EDGE('',*,*,#6333,.F.);
#9043=ORIENTED_EDGE('',*,*,#6335,.T.);
#9044=ORIENTED_EDGE('',*,*,#6336,.T.);
#9045=ORIENTED_EDGE('',*,*,#6337,.T.);
#9046=ORIENTED_EDGE('',*,*,#6335,.F.);
#9047=ORIENTED_EDGE('',*,*,#6338,.T.);
#9048=ORIENTED_EDGE('',*,*,#6339,.T.);
#9049=ORIENTED_EDGE('',*,*,#6340,.T.);
#9050=ORIENTED_EDGE('',*,*,#6336,.F.);
#9051=ORIENTED_EDGE('',*,*,#6337,.F.);
#9052=ORIENTED_EDGE('',*,*,#6340,.F.);
#9053=ORIENTED_EDGE('',*,*,#6338,.F.);
#9054=ORIENTED_EDGE('',*,*,#6339,.F.);
#9055=ORIENTED_EDGE('',*,*,#6341,.T.);
#9056=ORIENTED_EDGE('',*,*,#6342,.T.);
#9057=ORIENTED_EDGE('',*,*,#6341,.F.);
#9058=ORIENTED_EDGE('',*,*,#6343,.T.);
#9059=ORIENTED_EDGE('',*,*,#6342,.F.);
#9060=ORIENTED_EDGE('',*,*,#6343,.F.);
#9061=ORIENTED_EDGE('',*,*,#6344,.T.);
#9062=ORIENTED_EDGE('',*,*,#6318,.T.);
#9063=ORIENTED_EDGE('',*,*,#6344,.F.);
#9376=CYLINDRICAL_SURFACE('',#11117,19.);
#9377=CYLINDRICAL_SURFACE('',#11126,13.1);
#9378=CYLINDRICAL_SURFACE('',#11130,15.1);
#9379=CYLINDRICAL_SURFACE('',#11136,14.1);
#9380=CYLINDRICAL_SURFACE('',#11142,13.1);
#9381=CYLINDRICAL_SURFACE('',#11146,16.1);
#9894=ADVANCED_FACE('',(#1528,#546),#1004,.F.);
#9895=ADVANCED_FACE('',(#1529),#9376,.T.);
#9896=ADVANCED_FACE('',(#1530),#404,.F.);
#9897=ADVANCED_FACE('',(#1531),#365,.T.);
#9898=ADVANCED_FACE('',(#1532,#547),#1005,.F.);
#9899=ADVANCED_FACE('',(#1533),#9377,.F.);
#9900=ADVANCED_FACE('',(#1534,#548),#1006,.F.);
#9901=ADVANCED_FACE('',(#1535),#9378,.F.);
#9902=ADVANCED_FACE('',(#1536),#366,.F.);
#9903=ADVANCED_FACE('',(#1537),#9379,.F.);
#9904=ADVANCED_FACE('',(#1538),#367,.F.);
#9905=ADVANCED_FACE('',(#1539),#9380,.F.);
#9906=ADVANCED_FACE('',(#1540,#549),#1007,.F.);
#9907=ADVANCED_FACE('',(#1541),#9381,.F.);
#9964=CLOSED_SHELL('',(#9894,#9895,#9896,#9897,#9898,#9899,#9900,#9901,
#9902,#9903,#9904,#9905,#9906,#9907));
#11113=AXIS2_PLACEMENT_3D('',#32655,#13640,#13641);
#11114=AXIS2_PLACEMENT_3D('',#32656,#13642,#13643);
#11115=AXIS2_PLACEMENT_3D('',#32658,#13644,#13645);
#11116=AXIS2_PLACEMENT_3D('',#32660,#13646,#13647);
#11117=AXIS2_PLACEMENT_3D('',#32661,#13648,#13649);
#11118=AXIS2_PLACEMENT_3D('',#32664,#13651,#13652);
#11119=AXIS2_PLACEMENT_3D('',#32665,#13653,#13654);
#11120=AXIS2_PLACEMENT_3D('',#32667,#13655,#13656);
#11121=AXIS2_PLACEMENT_3D('',#32668,#13657,#13658);
#11122=AXIS2_PLACEMENT_3D('',#32669,#13659,#13660);
#11123=AXIS2_PLACEMENT_3D('',#32672,#13662,#13663);
#11124=AXIS2_PLACEMENT_3D('',#32673,#13664,#13665);
#11125=AXIS2_PLACEMENT_3D('',#32675,#13666,#13667);
#11126=AXIS2_PLACEMENT_3D('',#32676,#13668,#13669);
#11127=AXIS2_PLACEMENT_3D('',#32679,#13671,#13672);
#11128=AXIS2_PLACEMENT_3D('',#32680,#13673,#13674);
#11129=AXIS2_PLACEMENT_3D('',#32682,#13675,#13676);
#11130=AXIS2_PLACEMENT_3D('',#32683,#13677,#13678);
#11131=AXIS2_PLACEMENT_3D('',#32687,#13680,#13681);
#11132=AXIS2_PLACEMENT_3D('',#32688,#13682,#13683);
#11133=AXIS2_PLACEMENT_3D('',#32689,#13684,#13685);
#11134=AXIS2_PLACEMENT_3D('',#32692,#13686,#13687);
#11135=AXIS2_PLACEMENT_3D('',#32693,#13688,#13689);
#11136=AXIS2_PLACEMENT_3D('',#32695,#13691,#13692);
#11137=AXIS2_PLACEMENT_3D('',#32699,#13694,#13695);
#11138=AXIS2_PLACEMENT_3D('',#32700,#13696,#13697);
#11139=AXIS2_PLACEMENT_3D('',#32701,#13698,#13699);
#11140=AXIS2_PLACEMENT_3D('',#32704,#13700,#13701);
#11141=AXIS2_PLACEMENT_3D('',#32705,#13702,#13703);
#11142=AXIS2_PLACEMENT_3D('',#32707,#13705,#13706);
#11143=AXIS2_PLACEMENT_3D('',#32710,#13708,#13709);
#11144=AXIS2_PLACEMENT_3D('',#32711,#13710,#13711);
#11145=AXIS2_PLACEMENT_3D('',#32713,#13712,#13713);
#11146=AXIS2_PLACEMENT_3D('',#32714,#13714,#13715);
#13640=DIRECTION('axis',(0.,0.,1.));
#13641=DIRECTION('refdir',(1.,0.,0.));
#13642=DIRECTION('center_axis',(0.,1.,0.));
#13643=DIRECTION('ref_axis',(0.,0.,1.));
#13644=DIRECTION('center_axis',(0.,-1.,0.));
#13645=DIRECTION('ref_axis',(0.,0.,-1.));
#13646=DIRECTION('center_axis',(0.,-1.,0.));
#13647=DIRECTION('ref_axis',(0.,0.,-1.));
#13648=DIRECTION('center_axis',(0.,-1.,0.));
#13649=DIRECTION('ref_axis',(0.,0.,-1.));
#13650=DIRECTION('',(0.,1.,0.));
#13651=DIRECTION('center_axis',(0.,-1.,0.));
#13652=DIRECTION('ref_axis',(0.,0.,-1.));
#13653=DIRECTION('center_axis',(0.,-1.,0.));
#13654=DIRECTION('ref_axis',(0.,0.,-1.));
#13655=DIRECTION('center_axis',(1.,0.,1.22464679914735E-16));
#13656=DIRECTION('ref_axis',(-1.22464679914735E-16,0.,1.));
#13657=DIRECTION('center_axis',(0.,-1.,0.));
#13658=DIRECTION('ref_axis',(0.,0.,-1.));
#13659=DIRECTION('center_axis',(0.,-1.,0.));
#13660=DIRECTION('ref_axis',(0.,0.,-1.));
#13661=DIRECTION('',(2.97020476879948E-17,0.970142500145332,-0.242535625036333));
#13662=DIRECTION('center_axis',(0.,-1.,0.));
#13663=DIRECTION('ref_axis',(0.,0.,-1.));
#13664=DIRECTION('center_axis',(0.,-1.,0.));
#13665=DIRECTION('ref_axis',(0.,0.,-1.));
#13666=DIRECTION('center_axis',(0.,-1.,0.));
#13667=DIRECTION('ref_axis',(0.,0.,-1.));
#13668=DIRECTION('center_axis',(0.,-1.,0.));
#13669=DIRECTION('ref_axis',(0.,0.,-1.));
#13670=DIRECTION('',(0.,-1.,0.));
#13671=DIRECTION('center_axis',(0.,-1.,0.));
#13672=DIRECTION('ref_axis',(0.,0.,-1.));
#13673=DIRECTION('center_axis',(0.,1.,0.));
#13674=DIRECTION('ref_axis',(0.,0.,1.));
#13675=DIRECTION('center_axis',(0.,-1.,0.));
#13676=DIRECTION('ref_axis',(0.,0.,-1.));
#13677=DIRECTION('center_axis',(0.,-1.,0.));
#13678=DIRECTION('ref_axis',(0.,0.,-1.));
#13679=DIRECTION('',(0.,-1.,0.));
#13680=DIRECTION('center_axis',(0.,-1.,0.));
#13681=DIRECTION('ref_axis',(0.,0.,-1.));
#13682=DIRECTION('center_axis',(0.,-1.,0.));
#13683=DIRECTION('ref_axis',(0.,0.,-1.));
#13684=DIRECTION('center_axis',(0.,1.,0.));
#13685=DIRECTION('ref_axis',(0.,0.,1.));
#13686=DIRECTION('center_axis',(0.,-1.,0.));
#13687=DIRECTION('ref_axis',(0.,0.,-1.));
#13688=DIRECTION('center_axis',(0.,-1.,0.));
#13689=DIRECTION('ref_axis',(0.,0.,-1.));
#13690=DIRECTION('',(-8.65956056235495E-17,0.707106781186546,-0.707106781186549));
#13691=DIRECTION('center_axis',(0.,-1.,0.));
#13692=DIRECTION('ref_axis',(0.,0.,-1.));
#13693=DIRECTION('',(0.,-1.,0.));
#13694=DIRECTION('center_axis',(0.,-1.,0.));
#13695=DIRECTION('ref_axis',(0.,0.,-1.));
#13696=DIRECTION('center_axis',(0.,-1.,0.));
#13697=DIRECTION('ref_axis',(0.,0.,-1.));
#13698=DIRECTION('center_axis',(0.,1.,0.));
#13699=DIRECTION('ref_axis',(0.,0.,1.));
#13700=DIRECTION('center_axis',(0.,-1.,0.));
#13701=DIRECTION('ref_axis',(0.,0.,-1.));
#13702=DIRECTION('center_axis',(0.,-1.,0.));
#13703=DIRECTION('ref_axis',(0.,0.,-1.));
#13704=DIRECTION('',(-9.10089931823811E-17,0.669130606358856,-0.743144825477396));
#13705=DIRECTION('center_axis',(0.,-1.,0.));
#13706=DIRECTION('ref_axis',(0.,0.,-1.));
#13707=DIRECTION('',(0.,-1.,0.));
#13708=DIRECTION('center_axis',(0.,-1.,0.));
#13709=DIRECTION('ref_axis',(0.,0.,-1.));
#13710=DIRECTION('center_axis',(0.,1.,0.));
#13711=DIRECTION('ref_axis',(0.,0.,1.));
#13712=DIRECTION('center_axis',(0.,-1.,0.));
#13713=DIRECTION('ref_axis',(0.,0.,-1.));
#13714=DIRECTION('center_axis',(0.,-1.,0.));
#13715=DIRECTION('ref_axis',(0.,0.,-1.));
#13716=DIRECTION('',(0.,-1.,0.));
#32655=CARTESIAN_POINT('',(0.,0.,0.));
#32656=CARTESIAN_POINT('Origin',(-16.1,-2.1492551325036E-15,0.));
#32657=CARTESIAN_POINT('',(-2.32682891837997E-15,-2.32682891837997E-15,
19.));
#32658=CARTESIAN_POINT('Origin',(0.,-2.32682891837997E-15,0.));
#32659=CARTESIAN_POINT('',(-1.97168134662724E-15,-1.97168134662724E-15,
16.1));
#32660=CARTESIAN_POINT('Origin',(0.,-1.97168134662724E-15,0.));
#32661=CARTESIAN_POINT('Origin',(0.,0.,0.));
#32662=CARTESIAN_POINT('',(-2.32682891837997E-15,14.,19.));
#32663=CARTESIAN_POINT('',(-2.32682891837997E-15,0.,19.));
#32664=CARTESIAN_POINT('Origin',(0.,14.,0.));
#32665=CARTESIAN_POINT('Origin',(0.,27.2849025449883,0.));
#32666=CARTESIAN_POINT('',(-2.0818995585505E-15,28.,17.));
#32667=CARTESIAN_POINT('Origin',(-7.59211428773629E-15,27.2849025449883,
61.9943178149179));
#32668=CARTESIAN_POINT('Origin',(0.,28.,0.));
#32669=CARTESIAN_POINT('Origin',(0.,32.,0.));
#32670=CARTESIAN_POINT('',(-1.95943487863577E-15,32.,16.));
#32671=CARTESIAN_POINT('',(-1.95943487863577E-15,32.,16.));
#32672=CARTESIAN_POINT('Origin',(0.,32.,0.));
#32673=CARTESIAN_POINT('Origin',(-16.,32.,0.));
#32674=CARTESIAN_POINT('',(-1.60428730688303E-15,32.,13.1));
#32675=CARTESIAN_POINT('Origin',(0.,32.,0.));
#32676=CARTESIAN_POINT('Origin',(0.,0.,0.));
#32677=CARTESIAN_POINT('',(-1.60428730688303E-15,29.5,13.1));
#32678=CARTESIAN_POINT('',(-1.60428730688303E-15,0.,13.1));
#32679=CARTESIAN_POINT('Origin',(0.,29.5,0.));
#32680=CARTESIAN_POINT('Origin',(-13.1,29.5,0.));
#32681=CARTESIAN_POINT('',(-1.8492166667125E-15,29.5,15.1));
#32682=CARTESIAN_POINT('Origin',(0.,29.5,0.));
#32683=CARTESIAN_POINT('Origin',(0.,0.,0.));
#32684=CARTESIAN_POINT('',(-1.8492166667125E-15,23.9,15.1));
#32685=CARTESIAN_POINT('',(-1.8492166667125E-15,0.,15.1));
#32686=CARTESIAN_POINT('',(0.,23.9,-15.1));
#32687=CARTESIAN_POINT('Origin',(0.,23.9,0.));
#32688=CARTESIAN_POINT('Origin',(0.,23.9,0.));
#32689=CARTESIAN_POINT('Origin',(0.,22.9,0.));
#32690=CARTESIAN_POINT('',(0.,22.9,-14.1));
#32691=CARTESIAN_POINT('',(-1.72675198679777E-15,22.9,14.1));
#32692=CARTESIAN_POINT('Origin',(0.,22.9,0.));
#32693=CARTESIAN_POINT('Origin',(0.,22.9,0.));
#32694=CARTESIAN_POINT('',(-1.72675198679777E-15,22.9,-14.1));
#32695=CARTESIAN_POINT('Origin',(0.,0.,0.));
#32696=CARTESIAN_POINT('',(-1.72675198679777E-15,18.9,14.1));
#32697=CARTESIAN_POINT('',(-1.72675198679777E-15,0.,14.1));
#32698=CARTESIAN_POINT('',(0.,18.9,-14.1));
#32699=CARTESIAN_POINT('Origin',(0.,18.9,0.));
#32700=CARTESIAN_POINT('Origin',(0.,18.9,0.));
#32701=CARTESIAN_POINT('Origin',(0.,17.9995959557022,0.));
#32702=CARTESIAN_POINT('',(0.,17.9995959557022,-13.1));
#32703=CARTESIAN_POINT('',(-1.60428730688303E-15,17.9995959557022,13.1));
#32704=CARTESIAN_POINT('Origin',(0.,17.9995959557022,0.));
#32705=CARTESIAN_POINT('Origin',(0.,17.9995959557022,0.));
#32706=CARTESIAN_POINT('',(-1.60428730688303E-15,17.9995959557022,-13.1));
#32707=CARTESIAN_POINT('Origin',(0.,0.,0.));
#32708=CARTESIAN_POINT('',(-1.60428730688303E-15,16.,13.1));
#32709=CARTESIAN_POINT('',(-1.60428730688303E-15,0.,13.1));
#32710=CARTESIAN_POINT('Origin',(0.,16.,0.));
#32711=CARTESIAN_POINT('Origin',(-13.1,16.,0.));
#32712=CARTESIAN_POINT('',(-1.97168134662724E-15,16.,16.1));
#32713=CARTESIAN_POINT('Origin',(0.,16.,0.));
#32714=CARTESIAN_POINT('Origin',(0.,0.,0.));
#32715=CARTESIAN_POINT('',(-1.97168134662724E-15,0.,16.1));
#32979=UNCERTAINTY_MEASURE_WITH_UNIT(LENGTH_MEASURE(0.01),#33017,
'DISTANCE_ACCURACY_VALUE',
'Maximum model space distance between geometric entities at asserted c
onnectivities');
#32984=UNCERTAINTY_MEASURE_WITH_UNIT(LENGTH_MEASURE(0.01),#33017,
'DISTANCE_ACCURACY_VALUE',
'Maximum model space distance between geometric entities at asserted c
onnectivities');
#33011=(
GEOMETRIC_REPRESENTATION_CONTEXT(3)
GLOBAL_UNCERTAINTY_ASSIGNED_CONTEXT((#32979))
GLOBAL_UNIT_ASSIGNED_CONTEXT((#33017,#33019,#33020))
REPRESENTATION_CONTEXT('','3D')
);
#33016=(
GEOMETRIC_REPRESENTATION_CONTEXT(3)
GLOBAL_UNCERTAINTY_ASSIGNED_CONTEXT((#32984))
GLOBAL_UNIT_ASSIGNED_CONTEXT((#33017,#33019,#33020))
REPRESENTATION_CONTEXT('','3D')
);
#33017=(
LENGTH_UNIT()
NAMED_UNIT(*)
SI_UNIT(.MILLI.,.METRE.)
);
#33019=(
NAMED_UNIT(*)
PLANE_ANGLE_UNIT()
SI_UNIT($,.RADIAN.)
);
#33020=(
NAMED_UNIT(*)
SI_UNIT($,.STERADIAN.)
SOLID_ANGLE_UNIT()
);
#33047=SHAPE_DEFINITION_REPRESENTATION(#33100,#33150);
#33100=PRODUCT_DEFINITION_SHAPE('',$,#33182);
#33150=SHAPE_REPRESENTATION('',(#11113),#33011);
#33155=PRODUCT_DEFINITION_CONTEXT('part definition',#33250,'design');
#33182=PRODUCT_DEFINITION(
'P_Torque Wrench_Locking Ring_PRT-TQ-1012-05_M_Rev00','PRT-TQ-1012-04',
#33213,#33155);
#33213=PRODUCT_DEFINITION_FORMATION('',$,#33278);
#33250=APPLICATION_CONTEXT(
'Core Data for Automotive Mechanical Design Process');
#33251=PRODUCT_CONTEXT('part definition',#33250,'mechanical');
#33278=PRODUCT('P_Torque Wrench_Locking Ring_PRT-TQ-1012-05_M_Rev00',
'PRT-TQ-1012-04',$,(#33251));
#33284=PRESENTATION_STYLE_ASSIGNMENT((#33291));
#33291=SURFACE_STYLE_USAGE(.BOTH.,#33298);
#33298=SURFACE_SIDE_STYLE('',(#33305));
#33305=SURFACE_STYLE_FILL_AREA(#33312);
#33312=FILL_AREA_STYLE('Opaque(186,91,6)',(#33319));
#33319=FILL_AREA_STYLE_COLOUR('Opaque(186,91,6)',#33326);
#33326=COLOUR_RGB('Opaque(186,91,6)', 0.09019608, 0.27058824, 0.51372549);
ENDSEC;
END-ISO-10303-21;
